ISO-10303-21;
HEADER;
/* Generated by software containing ST-Developer
 * from STEP Tools, Inc. (www.steptools.com) 
 */

FILE_DESCRIPTION(
/* description */ ('Independent manual two-gate roller-track escapement for nominal30mm d
iameter20mm wide feed rollers. Opposed gates are driven by native capt
ured pin-slot loops with positive curved-slot travel stops at\X\B116de
g. Repeated gate/pin/washer/clip instances, adapted native common bear
ing families, full retaining lips and rotating polymer grip. External 
workpieces, gravity feeder/incline and mount anchors outside assembly.
 No powered-feed compatibility, impact, capacity, safety, force, wear 
or life rating.'),
/* implementation_level */ '2;1');

FILE_NAME(
/* name */ 'Stop thrust washer.step',
/* time_stamp */ '2026-11-08T18:43:23-08:00',
/* author */ (''),
/* organization */ (''),
/* preprocessor_version */ 'ST-DEVELOPER v20.2',
/* originating_system */ 'Autodesk Translation Framework v15.17.0.0',
/* authorisation */ '');

FILE_SCHEMA (('AUTOMOTIVE_DESIGN { 1 0 10303 214 3 1 1 }'));
ENDSEC;

DATA;
#10=MECHANICAL_DESIGN_GEOMETRIC_PRESENTATION_REPRESENTATION('',(#469),#19863);
#431=SHAPE_REPRESENTATION_RELATIONSHIP('SRR','None',#19949,#450);
#450=ADVANCED_BREP_SHAPE_REPRESENTATION('',(#488),#19858);
#469=STYLED_ITEM('',(#20043),#488);
#488=MANIFOLD_SOLID_BREP('Body1',#6438);
#864=LINE('',#15992,#1329);
#865=LINE('',#15998,#1330);
#1329=VECTOR('',#8356,2.);
#1330=VECTOR('',#8363,4.);
#1562=CYLINDRICAL_SURFACE('',#7048,2.);
#1563=CYLINDRICAL_SURFACE('',#7051,4.);
#1678=FACE_BOUND('',#2379,.T.);
#1679=FACE_BOUND('',#2381,.T.);
#1956=FACE_OUTER_BOUND('',#2376,.T.);
#1957=FACE_OUTER_BOUND('',#2377,.T.);
#1958=FACE_OUTER_BOUND('',#2378,.T.);
#1959=FACE_OUTER_BOUND('',#2380,.T.);
#2376=EDGE_LOOP('',(#5469,#5470,#5471,#5472));
#2377=EDGE_LOOP('',(#5473,#5474,#5475,#5476));
#2378=EDGE_LOOP('',(#5477));
#2379=EDGE_LOOP('',(#5478));
#2380=EDGE_LOOP('',(#5479));
#2381=EDGE_LOOP('',(#5480));
#2590=CIRCLE('',#7049,2.);
#2591=CIRCLE('',#7050,2.);
#2592=CIRCLE('',#7052,4.);
#2593=CIRCLE('',#7053,4.);
#3068=VERTEX_POINT('',#15989);
#3069=VERTEX_POINT('',#15991);
#3070=VERTEX_POINT('',#15995);
#3071=VERTEX_POINT('',#15997);
#3893=EDGE_CURVE('',#3068,#3068,#2590,.T.);
#3894=EDGE_CURVE('',#3068,#3069,#864,.T.);
#3895=EDGE_CURVE('',#3069,#3069,#2591,.T.);
#3896=EDGE_CURVE('',#3070,#3070,#2592,.T.);
#3897=EDGE_CURVE('',#3070,#3071,#865,.T.);
#3898=EDGE_CURVE('',#3071,#3071,#2593,.T.);
#5469=ORIENTED_EDGE('',*,*,#3893,.F.);
#5470=ORIENTED_EDGE('',*,*,#3894,.T.);
#5471=ORIENTED_EDGE('',*,*,#3895,.T.);
#5472=ORIENTED_EDGE('',*,*,#3894,.F.);
#5473=ORIENTED_EDGE('',*,*,#3896,.F.);
#5474=ORIENTED_EDGE('',*,*,#3897,.T.);
#5475=ORIENTED_EDGE('',*,*,#3898,.T.);
#5476=ORIENTED_EDGE('',*,*,#3897,.F.);
#5477=ORIENTED_EDGE('',*,*,#3896,.T.);
#5478=ORIENTED_EDGE('',*,*,#3893,.T.);
#5479=ORIENTED_EDGE('',*,*,#3898,.F.);
#5480=ORIENTED_EDGE('',*,*,#3895,.F.);
#6037=PLANE('',#7054);
#6038=PLANE('',#7055);
#6335=ADVANCED_FACE('',(#1956),#1562,.F.);
#6336=ADVANCED_FACE('',(#1957),#1563,.T.);
#6337=ADVANCED_FACE('',(#1958,#1678),#6037,.T.);
#6338=ADVANCED_FACE('',(#1959,#1679),#6038,.F.);
#6438=CLOSED_SHELL('',(#6335,#6336,#6337,#6338));
#7047=AXIS2_PLACEMENT_3D('',#15987,#8350,#8351);
#7048=AXIS2_PLACEMENT_3D('',#15988,#8352,#8353);
#7049=AXIS2_PLACEMENT_3D('',#15990,#8354,#8355);
#7050=AXIS2_PLACEMENT_3D('',#15993,#8357,#8358);
#7051=AXIS2_PLACEMENT_3D('',#15994,#8359,#8360);
#7052=AXIS2_PLACEMENT_3D('',#15996,#8361,#8362);
#7053=AXIS2_PLACEMENT_3D('',#15999,#8364,#8365);
#7054=AXIS2_PLACEMENT_3D('',#16000,#8366,#8367);
#7055=AXIS2_PLACEMENT_3D('',#16001,#8368,#8369);
#8350=DIRECTION('axis',(0.,0.,1.));
#8351=DIRECTION('refdir',(1.,0.,0.));
#8352=DIRECTION('center_axis',(0.,0.,1.));
#8353=DIRECTION('ref_axis',(1.,0.,0.));
#8354=DIRECTION('center_axis',(0.,0.,-1.));
#8355=DIRECTION('ref_axis',(1.,0.,0.));
#8356=DIRECTION('',(0.,0.,-1.));
#8357=DIRECTION('center_axis',(0.,0.,-1.));
#8358=DIRECTION('ref_axis',(1.,0.,0.));
#8359=DIRECTION('center_axis',(0.,0.,1.));
#8360=DIRECTION('ref_axis',(1.,0.,0.));
#8361=DIRECTION('center_axis',(0.,0.,1.));
#8362=DIRECTION('ref_axis',(1.,0.,0.));
#8363=DIRECTION('',(0.,0.,-1.));
#8364=DIRECTION('center_axis',(0.,0.,1.));
#8365=DIRECTION('ref_axis',(1.,0.,0.));
#8366=DIRECTION('center_axis',(0.,0.,1.));
#8367=DIRECTION('ref_axis',(1.,0.,0.));
#8368=DIRECTION('center_axis',(0.,0.,1.));
#8369=DIRECTION('ref_axis',(1.,0.,0.));
#15987=CARTESIAN_POINT('',(0.,0.,0.));
#15988=CARTESIAN_POINT('Origin',(0.,0.,0.));
#15989=CARTESIAN_POINT('',(-2.,-2.44929359829471E-16,1.));
#15990=CARTESIAN_POINT('Origin',(0.,0.,1.));
#15991=CARTESIAN_POINT('',(-2.,-2.44929359829471E-16,0.));
#15992=CARTESIAN_POINT('',(-2.,-2.44929359829471E-16,0.));
#15993=CARTESIAN_POINT('Origin',(0.,0.,0.));
#15994=CARTESIAN_POINT('Origin',(0.,0.,0.));
#15995=CARTESIAN_POINT('',(-4.,-4.89858719658941E-16,1.));
#15996=CARTESIAN_POINT('Origin',(0.,0.,1.));
#15997=CARTESIAN_POINT('',(-4.,-4.89858719658941E-16,0.));
#15998=CARTESIAN_POINT('',(-4.,-4.89858719658941E-16,0.));
#15999=CARTESIAN_POINT('Origin',(0.,0.,0.));
#16000=CARTESIAN_POINT('Origin',(0.,0.,1.));
#16001=CARTESIAN_POINT('Origin',(0.,0.,0.));
#19837=UNCERTAINTY_MEASURE_WITH_UNIT(LENGTH_MEASURE(0.01),#19864,
'DISTANCE_ACCURACY_VALUE',
'Maximum model space distance between geometric entities at asserted c
onnectivities');
#19842=UNCERTAINTY_MEASURE_WITH_UNIT(LENGTH_MEASURE(0.01),#19864,
'DISTANCE_ACCURACY_VALUE',
'Maximum model space distance between geometric entities at asserted c
onnectivities');
#19858=(
GEOMETRIC_REPRESENTATION_CONTEXT(3)
GLOBAL_UNCERTAINTY_ASSIGNED_CONTEXT((#19837))
GLOBAL_UNIT_ASSIGNED_CONTEXT((#19864,#19866,#19867))
REPRESENTATION_CONTEXT('','3D')
);
#19863=(
GEOMETRIC_REPRESENTATION_CONTEXT(3)
GLOBAL_UNCERTAINTY_ASSIGNED_CONTEXT((#19842))
GLOBAL_UNIT_ASSIGNED_CONTEXT((#19864,#19866,#19867))
REPRESENTATION_CONTEXT('','3D')
);
#19864=(
LENGTH_UNIT()
NAMED_UNIT(*)
SI_UNIT(.MILLI.,.METRE.)
);
#19866=(
NAMED_UNIT(*)
PLANE_ANGLE_UNIT()
SI_UNIT($,.RADIAN.)
);
#19867=(
NAMED_UNIT(*)
SI_UNIT($,.STERADIAN.)
SOLID_ANGLE_UNIT()
);
#19883=SHAPE_DEFINITION_REPRESENTATION(#19903,#19949);
#19903=PRODUCT_DEFINITION_SHAPE('',$,#19970);
#19949=SHAPE_REPRESENTATION('',(#7047),#19858);
#19954=PRODUCT_DEFINITION_CONTEXT('part definition',#20016,'design');
#19970=PRODUCT_DEFINITION('Stop thrust washer','Stop thrust washer',#19990,
#19954);
#19990=PRODUCT_DEFINITION_FORMATION('',$,#20033);
#20016=APPLICATION_CONTEXT(
'Core Data for Automotive Mechanical Design Process');
#20017=PRODUCT_CONTEXT('part definition',#20016,'mechanical');
#20033=PRODUCT('Stop thrust washer','Stop thrust washer',$,(#20017));
#20043=PRESENTATION_STYLE_ASSIGNMENT((#20050));
#20050=SURFACE_STYLE_USAGE(.BOTH.,#20057);
#20057=SURFACE_SIDE_STYLE('',(#20064));
#20064=SURFACE_STYLE_FILL_AREA(#20071);
#20071=FILL_AREA_STYLE('Light gray',(#20078));
#20078=FILL_AREA_STYLE_COLOUR('Light gray',#20085);
#20085=COLOUR_RGB('Light gray',0.725490196078431,0.752941176470588,0.792156862745098);
ENDSEC;
END-ISO-10303-21;
